ISO-10303-21;
HEADER;
FILE_DESCRIPTION (('STEP AP203'),
    '1' );
FILE_NAME ('Aloris-BXA-Wedge-R.step',
    '2026-10-07T20:09:13',
    ( '' ),
    ( '' ),
    'SwSTEP 2.0',
    'SolidWorks 2024',
    '' );
FILE_SCHEMA (( 'AUTOMOTIVE_DESIGN' ));
ENDSEC;

DATA;
#35=CARTESIAN_POINT ( 'NONE',  ( -0.3616234456863465230, 3.514980167629567998, 2.635972749958888528 ) ) ;
#76=CARTESIAN_POINT ( 'NONE',  ( -0.4316174467094854306, 0.9548081934128058723, 2.771794876808019836 ) ) ;
#124=EDGE_CURVE ( 'NONE', #17018, #2833, #252, .T. ) ;
#173=ORIENTED_EDGE ( 'NONE', *, *, #22442, .F. ) ;
#252=LINE ( 'NONE', #17321, #13881 ) ;
#283=CARTESIAN_POINT ( 'NONE',  ( 0.3003475124358242487, 3.066692553488282957, 3.638968604327563749 ) ) ;
#287=VECTOR ( 'NONE', #16443, 39.37007874015748854 ) ;
#289=DIRECTION ( 'NONE',  ( -0.8660254037844382635, 0.000000000000000000, -0.5000000000000004441 ) ) ;
#321=DIRECTION ( 'NONE',  ( -0.8660254037844443697, 0.000000000000000000, -0.4999999999999902300 ) ) ;
#423=DIRECTION ( 'NONE',  ( 0.000000000000000000, 0.000000000000000000, -1.000000000000000000 ) ) ;
#443=LINE ( 'NONE', #11554, #17647 ) ;
#582=PRODUCT_DEFINITION_FORMATION_WITH_SPECIFIED_SOURCE ( 'ANY', '', #12267, .NOT_KNOWN. ) ;
#767=ORIENTED_EDGE ( 'NONE', *, *, #8582, .F. ) ;
#914=CARTESIAN_POINT ( 'NONE',  ( -0.1166234456863465552, 3.066692553488282957, 2.777423565910347225 ) ) ;
#995=EDGE_CURVE ( 'NONE', #21184, #3065, #22681, .T. ) ;
#1015=CARTESIAN_POINT ( 'NONE',  ( -0.5116234456863466562, 0.4427737985694512046, 2.618652241883199228 ) ) ;
#1044=MANIFOLD_SOLID_BREP ( 'Body-Move/Copy1', #3742 ) ;
#1126=VECTOR ( 'NONE', #2279, 39.37007874015748854 ) ;
#1137=CARTESIAN_POINT ( 'NONE',  ( -0.5116234456863466562, 3.514980167629567998, 2.722575290337332365 ) ) ;
#1141=PLANE ( 'NONE',  #20540 ) ;
#1159=CARTESIAN_POINT ( 'NONE',  ( -0.1166234456863465552, 0.9548081934128058723, 2.777423565910347225 ) ) ;
#1254=PLANE ( 'NONE',  #14415 ) ;
#1336=AXIS2_PLACEMENT_3D ( 'NONE', #7411, #5575, #3751 ) ;
#1378=CARTESIAN_POINT ( 'NONE',  ( -0.4366234456863466451, 0.9548081934128056503, 2.592671479769666387 ) ) ;
#1449=DIRECTION ( 'NONE',  ( -0.8660254037844420383, 0.000000000000000000, -0.4999999999999942268 ) ) ;
#1480=VECTOR ( 'NONE', #4022, 39.37007874015748143 ) ;
#1484=LINE ( 'NONE', #8793, #21573 ) ;
#1494=ORIENTED_EDGE ( 'NONE', *, *, #5186, .T. ) ;
#1495=DIRECTION ( 'NONE',  ( -0.4999999999999916178, 0.000000000000000000, 0.8660254037844434816 ) ) ;
#1497=CARTESIAN_POINT ( 'NONE',  ( -0.3466234456863465652, 4.027014562472920112, 2.644633003996732512 ) ) ;
#1501=FACE_OUTER_BOUND ( 'NONE', #19616, .T. ) ;
#1528=DIRECTION ( 'NONE',  ( -0.8660254037844377084, 0.000000000000000000, -0.5000000000000015543 ) ) ;
#1552=LINE ( 'NONE', #76, #8296 ) ;
#1590=EDGE_CURVE ( 'NONE', #8012, #7081, #24034, .T. ) ;
#1679=CARTESIAN_POINT ( 'NONE',  ( -0.5116234456863466562, 1.808198851485059100, 2.664840263418369659 ) ) ;
#1687=DIRECTION ( 'NONE',  ( 0.000000000000000000, 1.000000000000000000, 0.000000000000000000 ) ) ;
#1695=CARTESIAN_POINT ( 'NONE',  ( -0.1166234456863465552, 0.9548081934128058723, 2.711183489075826181 ) ) ;
#1713=DIRECTION ( 'NONE',  ( -0.8660254037844437036, 0.000000000000000000, -0.4999999999999913403 ) ) ;
#1717=DIRECTION ( 'NONE',  ( 0.5000000000000003331, 0.000000000000000000, -0.8660254037844383745 ) ) ;
#1760=CARTESIAN_POINT ( 'NONE',  ( 0.2730879860166530726, 0.9548081934128058723, 2.751417548891517573 ) ) ;
#1798=LINE ( 'NONE', #12801, #287 ) ;
#1832=CARTESIAN_POINT ( 'NONE',  ( 1.131433074307491404, 3.066692553488282957, 0.8537320438460626049 ) ) ;
#1998=ORIENTED_EDGE ( 'NONE', *, *, #124, .F. ) ;
#2058=DIRECTION ( 'NONE',  ( 0.000000000000000000, 0.000000000000000000, 1.000000000000000000 ) ) ;
#2074=LINE ( 'NONE', #7915, #19209 ) ;
#2147=ORIENTED_EDGE ( 'NONE', *, *, #22390, .F. ) ;
#2174=LINE ( 'NONE', #13282, #20158 ) ;
#2246=CARTESIAN_POINT ( 'NONE',  ( -0.02441201398334205686, 3.066692553488282957, 3.451468604327566858 ) ) ;
#2273=VERTEX_POINT ( 'NONE', #14766 ) ;
#2279=DIRECTION ( 'NONE',  ( 0.4999999999999915068, 0.000000000000000000, -0.8660254037844434816 ) ) ;
#2297=ORIENTED_EDGE ( 'NONE', *, *, #6038, .F. ) ;
#2307=ORIENTED_EDGE ( 'NONE', *, *, #5269, .T. ) ;
#2330=CARTESIAN_POINT ( 'NONE',  ( 0.7108475124358174524, 3.066692553488282957, 2.927961747820534644 ) ) ;
#2370=LINE ( 'NONE', #11516, #12422 ) ;
#2374=ORIENTED_EDGE ( 'NONE', *, *, #7635, .F. ) ;
#2465=AXIS2_PLACEMENT_3D ( 'NONE', #4945, #12289, #19463 ) ;
#2523=EDGE_LOOP ( 'NONE', ( #17996, #19138, #13813, #19199 ) ) ;
#2652=VERTEX_POINT ( 'NONE', #12307 ) ;
#2659=VECTOR ( 'NONE', #20803, 39.37007874015748143 ) ;
#2713=VECTOR ( 'NONE', #1717, 39.37007874015748143 ) ;
#2833=VERTEX_POINT ( 'NONE', #17368 ) ;
#2860=ADVANCED_FACE ( 'NONE', ( #10652 ), #1141, .T. ) ;
#2873=PLANE ( 'NONE',  #2465 ) ;
#2936=LINE ( 'NONE', #5115, #22346 ) ;
#2959=ORIENTED_EDGE ( 'NONE', *, *, #9659, .T. ) ;
#2984=ORIENTED_EDGE ( 'NONE', *, *, #14455, .T. ) ;
#3065=VERTEX_POINT ( 'NONE', #12616 ) ;
#3093=DIRECTION ( 'NONE',  ( 0.8660254037844435926, 0.000000000000000000, 0.4999999999999914513 ) ) ;
#3190=ORIENTED_EDGE ( 'NONE', *, *, #16584, .F. ) ;
#3200=CARTESIAN_POINT ( 'NONE',  ( -0.5116234456863466562, 4.027014562472920112, 2.549370209580444691 ) ) ;
#3228=CARTESIAN_POINT ( 'NONE',  ( -0.5116234456863466562, -0.003009961218012348859, 2.549370209580444246 ) ) ;
#3245=FACE_OUTER_BOUND ( 'NONE', #23069, .T. ) ;
#3310=EDGE_CURVE ( 'NONE', #13148, #21887, #1798, .T. ) ;
#3392=CARTESIAN_POINT ( 'NONE',  ( -0.1060554323913586589, -0.003009961218012348859, 2.783525011231007706 ) ) ;
#3399=EDGE_CURVE ( 'NONE', #8579, #7867, #2174, .T. ) ;
#3414=ORIENTED_EDGE ( 'NONE', *, *, #23741, .F. ) ;
#3462=ORIENTED_EDGE ( 'NONE', *, *, #16584, .T. ) ;
#3535=FACE_OUTER_BOUND ( 'NONE', #9691, .T. ) ;
#3543=VECTOR ( 'NONE', #14254, 39.37007874015748854 ) ;
#3555=EDGE_LOOP ( 'NONE', ( #22008, #767, #13904, #22904, #17198, #11031 ) ) ;
#3559=CARTESIAN_POINT ( 'NONE',  ( -0.5116234456863466562, 1.808198851485059988, 2.549370209580444691 ) ) ;
#3583=CARTESIAN_POINT ( 'NONE',  ( -0.1166234456863465552, 3.066692553488282957, 2.711183489075826181 ) ) ;
#3623=PLANE ( 'NONE',  #1336 ) ;
#3633=ORIENTED_EDGE ( 'NONE', *, *, #13120, .F. ) ;
#3742=CLOSED_SHELL ( 'NONE', ( #4111, #9837, #17596, #2860, #19851, #10733, #13501, #22727, #19441, #9629, #12004, #16611, #8942, #23112, #13635, #5190, #10403 ) ) ;
#3751=DIRECTION ( 'NONE',  ( 0.4999999999999916178, 0.000000000000000000, -0.8660254037844433705 ) ) ;
#3843=DIRECTION ( 'NONE',  ( 0.000000000000000000, -0.9961946980917454342, -0.08715574274765842955 ) ) ;
#3888=ORIENTED_EDGE ( 'NONE', *, *, #20650, .T. ) ;
#3960=CARTESIAN_POINT ( 'NONE',  ( 0.008081987039794995969, 0.9548081934128058723, 3.210421403429992271 ) ) ;
#4022=DIRECTION ( 'NONE',  ( 0.000000000000000000, -0.9961946980917454342, -0.08715574274765833240 ) ) ;
#4111=ADVANCED_FACE ( 'NONE', ( #8551 ), #16114, .T. ) ;
#4140=DIRECTION ( 'NONE',  ( 0.000000000000000000, 0.000000000000000000, -1.000000000000000000 ) ) ;
#4150=CARTESIAN_POINT ( 'NONE',  ( 0.3860879860166477329, 3.066692553488282957, 2.740461747820544414 ) ) ;
#4180=ORIENTED_EDGE ( 'NONE', *, *, #24068, .F. ) ;
#4196=DIRECTION ( 'NONE',  ( -0.4999999999999908962, 0.000000000000000000, 0.8660254037844438146 ) ) ;
#4201=LINE ( 'NONE', #11653, #19195 ) ;
#4227=EDGE_CURVE ( 'NONE', #21772, #5544, #11108, .T. ) ;
#4232=DIRECTION ( 'NONE',  ( 0.000000000000000000, 1.000000000000000000, 0.000000000000000000 ) ) ;
#4302=EDGE_LOOP ( 'NONE', ( #22602, #14794, #10102, #10681, #2959, #4180 ) ) ;
#4382=EDGE_CURVE ( 'NONE', #21772, #13133, #11471, .T. ) ;
#4390=LINE ( 'NONE', #4150, #13435 ) ;
#4401=VECTOR ( 'NONE', #10688, 39.37007874015748143 ) ;
#4451=DIRECTION ( 'NONE',  ( 0.000000000000000000, 1.000000000000000000, 0.000000000000000000 ) ) ;
#4469=CARTESIAN_POINT ( 'NONE',  ( -0.3616234456863465230, 3.514980167629567998, 2.635972749958888528 ) ) ;
#4585=EDGE_LOOP ( 'NONE', ( #22779, #13479, #12087, #3462 ) ) ;
#4597=CARTESIAN_POINT ( 'NONE',  ( -0.5116234456863466562, 0.9548081934128183068, 2.549370209580444246 ) ) ;
#4743=ADVANCED_BREP_SHAPE_REPRESENTATION ( '', ( #1044, #9127 ), #5239 ) ;
#4791=CARTESIAN_POINT ( 'NONE',  ( -0.4366234456863467006, 0.9548081934128058723, 2.592671479769666387 ) ) ;
#4907=EDGE_LOOP ( 'NONE', ( #11581, #4951, #10524, #2307 ) ) ;
#4910=CARTESIAN_POINT ( 'NONE',  ( -0.5116234456863466562, 0.9548081934128056503, 2.635972749958888528 ) ) ;
#4945=CARTESIAN_POINT ( 'NONE',  ( -0.09435543239135868454, -0.003009961218012348859, 2.763260016782451700 ) ) ;
#4951=ORIENTED_EDGE ( 'NONE', *, *, #20650, .F. ) ;
#5042=ORIENTED_EDGE ( 'NONE', *, *, #23927, .T. ) ;
#5061=LINE ( 'NONE', #12531, #4401 ) ;
#5115=CARTESIAN_POINT ( 'NONE',  ( -0.5116234456863466562, 3.066692553488282957, 2.910369331946250249 ) ) ;
#5132=( NAMED_UNIT ( * ) SI_UNIT ( $, .STERADIAN. ) SOLID_ANGLE_UNIT ( ) );
#5144=CARTESIAN_POINT ( 'NONE',  ( -0.4466234456863466540, 0.6134519301839026495, 2.586897977077770250 ) ) ;
#5165=VERTEX_POINT ( 'NONE', #17385 ) ;
#5186=EDGE_CURVE ( 'NONE', #5448, #7946, #10080, .T. ) ;
#5190=ADVANCED_FACE ( 'NONE', ( #23093 ), #17623, .F. ) ;
#5239=( GEOMETRIC_REPRESENTATION_CONTEXT ( 3 ) GLOBAL_UNCERTAINTY_ASSIGNED_CONTEXT ( ( #19473 ) ) GLOBAL_UNIT_ASSIGNED_CONTEXT ( ( #12478, #18310, #5132 ) ) REPRESENTATION_CONTEXT ( 'NONE', 'WORKASPACE' ) );
#5269=EDGE_CURVE ( 'NONE', #21887, #2273, #15555, .T. ) ;
#5288=AXIS2_PLACEMENT_3D ( 'NONE', #3228, #22003, #10678 ) ;
#5390=CARTESIAN_POINT ( 'NONE',  ( -0.4116234456863466229, 1.808198851485059988, 2.607105236499406953 ) ) ;
#5394=CARTESIAN_POINT ( 'NONE',  ( -0.5116234456863466562, 3.066692553488282957, 2.754369331946250110 ) ) ;
#5438=CARTESIAN_POINT ( 'NONE',  ( -0.001863919267180048824, 3.066692553488282957, 2.816660016782450704 ) ) ;
#5448=VERTEX_POINT ( 'NONE', #1159 ) ;
#5544=VERTEX_POINT ( 'NONE', #3583 ) ;
#5575=DIRECTION ( 'NONE',  ( -0.8651979924482661177, 0.04370253788966847741, -0.4995222938423191095 ) ) ;
#5625=LINE ( 'NONE', #16493, #21756 ) ;
#5651=CARTESIAN_POINT ( 'NONE',  ( -0.4366234456863467006, 0.9548081934128058723, 2.592671479769666387 ) ) ;
#5743=EDGE_CURVE ( 'NONE', #10641, #6836, #2370, .T. ) ;
#5745=CARTESIAN_POINT ( 'NONE',  ( -0.09435543239135868454, 3.514980167629567998, 2.763260016782451700 ) ) ;
#5767=CARTESIAN_POINT ( 'NONE',  ( -0.001863919267180048824, 3.514980167629567998, 2.816660016782450704 ) ) ;
#5857=DIRECTION ( 'NONE',  ( 0.8660254037844434816, 0.000000000000000000, 0.4999999999999916178 ) ) ;
#5863=ORIENTED_EDGE ( 'NONE', *, *, #16177, .F. ) ;
#5866=CARTESIAN_POINT ( 'NONE',  ( 0.7108475124358174524, 3.066692553488282957, 2.927961747820534644 ) ) ;
#5921=DIRECTION ( 'NONE',  ( 0.000000000000000000, -0.9961946980917454342, -0.08715574274765833240 ) ) ;
#5923=CARTESIAN_POINT ( 'NONE',  ( -0.02441201398334205686, 3.066692553488282957, 3.451468604327566858 ) ) ;
#5950=DIRECTION ( 'NONE',  ( 0.000000000000000000, 0.000000000000000000, 1.000000000000000000 ) ) ;
#5966=DIRECTION ( 'NONE',  ( -0.4999999999999942268, 0.000000000000000000, 0.8660254037844420383 ) ) ;
#6038=EDGE_CURVE ( 'NONE', #9585, #21966, #5625, .T. ) ;
#6052=AXIS2_PLACEMENT_3D ( 'NONE', #5923, #17025, #22638 ) ;
#6090=DIRECTION ( 'NONE',  ( 0.000000000000000000, -0.9961946980917454342, -0.08715574274765833240 ) ) ;
#6156=ORIENTED_EDGE ( 'NONE', *, *, #20625, .F. ) ;
#6277=EDGE_CURVE ( 'NONE', #21887, #10641, #14390, .T. ) ;
#6288=CARTESIAN_POINT ( 'NONE',  ( -0.5116234456863466562, 3.514980167629567998, 2.949589416182695878 ) ) ;
#6679=ORIENTED_EDGE ( 'NONE', *, *, #22252, .T. ) ;
#6836=VERTEX_POINT ( 'NONE', #20899 ) ;
#6847=ORIENTED_EDGE ( 'NONE', *, *, #19239, .T. ) ;
#6869=EDGE_LOOP ( 'NONE', ( #1998, #3190, #12460, #3888 ) ) ;
#6983=EDGE_LOOP ( 'NONE', ( #11840, #13353, #5042, #2297 ) ) ;
#6987=CARTESIAN_POINT ( 'NONE',  ( -0.5116234456863466562, 3.685658299244018554, 2.549370209580444691 ) ) ;
#7081=VERTEX_POINT ( 'NONE', #24100 ) ;
#7115=DIRECTION ( 'NONE',  ( 0.000000000000000000, 0.000000000000000000, -1.000000000000000000 ) ) ;
#7120=CARTESIAN_POINT ( 'NONE',  ( -0.7171867353193368544, 0.9548081934128058723, 2.866728992292166378 ) ) ;
#7168=ORIENTED_EDGE ( 'NONE', *, *, #13359, .F. ) ;
#7229=CARTESIAN_POINT ( 'NONE',  ( -0.5116234456863466562, 0.6134519301839024275, 2.549370209580444691 ) ) ;
#7290=ORIENTED_EDGE ( 'NONE', *, *, #23927, .F. ) ;
#7293=FACE_OUTER_BOUND ( 'NONE', #4585, .T. ) ;
#7381=VERTEX_POINT ( 'NONE', #16388 ) ;
#7411=CARTESIAN_POINT ( 'NONE',  ( 0.3860879860166477329, 3.066692553488282957, 2.740461747820544414 ) ) ;
#7414=CARTESIAN_POINT ( 'NONE',  ( -0.5116234456863466562, 0.9548081934128058723, 2.635972749958888528 ) ) ;
#7511=CARTESIAN_POINT ( 'NONE',  ( -0.5116234456863466562, 0.9548081934128058723, 2.549370209580444246 ) ) ;
#7635=EDGE_CURVE ( 'NONE', #5544, #7381, #21804, .T. ) ;
#7720=AXIS2_PLACEMENT_3D ( 'NONE', #7989, #4451, #7870 ) ;
#7747=ORIENTED_EDGE ( 'NONE', *, *, #21127, .T. ) ;
#7779=ORIENTED_EDGE ( 'NONE', *, *, #17225, .T. ) ;
#7788=VECTOR ( 'NONE', #1528, 39.37007874015748854 ) ;
#7867=VERTEX_POINT ( 'NONE', #16810 ) ;
#7870=DIRECTION ( 'NONE',  ( 0.000000000000000000, 0.000000000000000000, -1.000000000000000000 ) ) ;
#7913=CARTESIAN_POINT ( 'NONE',  ( 0.2730879860166530726, 3.066692553488282957, 2.936183489075822717 ) ) ;
#7915=CARTESIAN_POINT ( 'NONE',  ( 1.038941561183303497, 3.066692553488282957, 0.8003320438460471697 ) ) ;
#7946=VERTEX_POINT ( 'NONE', #14319 ) ;
#7989=CARTESIAN_POINT ( 'NONE',  ( -0.7171867353193368544, 0.9548081934128058723, 2.866728992292166378 ) ) ;
#8012=VERTEX_POINT ( 'NONE', #23680 ) ;
#8193=( BOUNDED_SURFACE ( )  B_SPLINE_SURFACE ( 2, 3, ( 
 ( #1015, #15890, #17846, #4910, #23310, #14068, #1137, #8572, #16013, #23431 ),
 ( #21616, #7229, #19911, #12611, #3559, #12855, #12490, #6987, #11129, #3200 ),
 ( #20029, #5144, #18078, #1378, #5390, #8807, #18201, #14675, #20272, #1497 ) ),
 .UNSPECIFIED., .F., .F., .T. ) 
 B_SPLINE_SURFACE_WITH_KNOTS ( ( 3, 3 ),
 ( 4, 3, 3, 4 ),
 ( 0.000000000000000000, 1.000000000000000000 ),
 ( 0.01132290749860157507, 0.02432858112762278230, 0.08935694927272853916, 0.1023626229017496891 ),
 .UNSPECIFIED. ) 
 GEOMETRIC_REPRESENTATION_ITEM ( )  RATIONAL_B_SPLINE_SURFACE ( (
 ( 1.000000000000000000, 1.000000000000000000, 1.000000000000000000, 1.000000000000000000, 1.000000000000000000, 1.000000000000000000, 1.000000000000000000, 1.000000000000000000, 1.000000000000000000, 1.000000000000000000),
 ( 0.4999999999999997780, 0.4999999999999997780, 0.4999999999999997780, 0.4999999999999997780, 0.4999999999999997780, 0.4999999999999997780, 0.4999999999999997780, 0.4999999999999997780, 0.4999999999999997780, 0.4999999999999997780),
 ( 1.000000000000000000, 1.000000000000000000, 1.000000000000000000, 1.000000000000000000, 1.000000000000000000, 1.000000000000000000, 1.000000000000000000, 1.000000000000000000, 1.000000000000000000, 1.000000000000000000) ) ) 
 REPRESENTATION_ITEM ( '' )  SURFACE ( )  );
#8275=ORIENTED_EDGE ( 'NONE', *, *, #14455, .F. ) ;
#8296=VECTOR ( 'NONE', #8989, 39.37007874015748854 ) ;
#8340=ORIENTED_EDGE ( 'NONE', *, *, #13120, .T. ) ;
#8342=CARTESIAN_POINT ( 'NONE',  ( 0.3003475124358242487, 3.066692553488282957, 3.638968604327563749 ) ) ;
#8412=CARTESIAN_POINT ( 'NONE',  ( 0.7108475124358174524, 3.066692553488282957, 2.927961747820534644 ) ) ;
#8468=EDGE_CURVE ( 'NONE', #7081, #9585, #18542, .T. ) ;
#8537=DIRECTION ( 'NONE',  ( 0.4985709748471340297, 0.07555085810113193467, -0.8635502596144368770 ) ) ;
#8550=PRODUCT_DEFINITION_SHAPE ( 'NONE', 'NONE',  #10901 ) ;
#8551=FACE_OUTER_BOUND ( 'NONE', #3555, .T. ) ;
#8572=CARTESIAN_POINT ( 'NONE',  ( -0.5116234456863466562, 3.685658299244018998, 2.728348793029228059 ) ) ;
#8579=VERTEX_POINT ( 'NONE', #22797 ) ;
#8582=EDGE_CURVE ( 'NONE', #5165, #2652, #13198, .T. ) ;
#8658=CARTESIAN_POINT ( 'NONE',  ( -0.5116234456863466562, 3.514980167629567998, 2.722575290337332365 ) ) ;
#8750=CARTESIAN_POINT ( 'NONE',  ( -0.1166234456863465552, 3.066692553488282957, 2.711183489075826181 ) ) ;
#8793=CARTESIAN_POINT ( 'NONE',  ( -0.5116234456863466562, 3.514980167629567998, 2.549370209580444246 ) ) ;
#8801=ORIENTED_EDGE ( 'NONE', *, *, #4382, .T. ) ;
#8807=CARTESIAN_POINT ( 'NONE',  ( -0.3866234456863466007, 2.661589509557314326, 2.621538993229147962 ) ) ;
#8836=PLANE ( 'NONE',  #5288 ) ;
#8888=VECTOR ( 'NONE', #5921, 39.37007874015748143 ) ;
#8896=CARTESIAN_POINT ( 'NONE',  ( 0.3003475124358242487, 3.066692553488282957, 3.638968604327563749 ) ) ;
#8936=PLANE ( 'NONE',  #18309 ) ;
#8942=ADVANCED_FACE ( 'NONE', ( #16210 ), #20228, .T. ) ;
#8989=DIRECTION ( 'NONE',  ( 0.8660254037844437036, 0.000000000000000000, 0.4999999999999910627 ) ) ;
#9028=CARTESIAN_POINT ( 'NONE',  ( -0.3616234456863465230, 3.514980167629567998, 2.635972749958888528 ) ) ;
#9094=EDGE_LOOP ( 'NONE', ( #23525, #20294, #15294, #7290, #2147, #6156, #9798 ) ) ;
#9111=LINE ( 'NONE', #16561, #15214 ) ;
#9112=CARTESIAN_POINT ( 'NONE',  ( -0.5116234456863466562, 3.514980167629567998, 2.722575290337332365 ) ) ;
#9122=DIRECTION ( 'NONE',  ( 0.000000000000000000, 0.000000000000000000, -1.000000000000000000 ) ) ;
#9127=AXIS2_PLACEMENT_3D ( 'NONE', #15878, #23181, #23294 ) ;
#9267=DIRECTION ( 'NONE',  ( -0.8651979924482665618, 0.04370253788966840108, -0.4995222938423183878 ) ) ;
#9311=CARTESIAN_POINT ( 'NONE',  ( -0.4116234456863466229, 1.808198851485060210, 2.607105236499406953 ) ) ;
#9323=CARTESIAN_POINT ( 'NONE',  ( -0.02441201398334205686, 3.066692553488282957, 3.451468604327566858 ) ) ;
#9427=ORIENTED_EDGE ( 'NONE', *, *, #8468, .T. ) ;
#9563=LINE ( 'NONE', #13005, #20688 ) ;
#9585=VERTEX_POINT ( 'NONE', #5438 ) ;
#9629=ADVANCED_FACE ( 'NONE', ( #3245 ), #10693, .F. ) ;
#9631=PLANE ( 'NONE',  #20784 ) ;
#9659=EDGE_CURVE ( 'NONE', #5448, #21184, #18848, .T. ) ;
#9691=EDGE_LOOP ( 'NONE', ( #24010, #18835, #3633, #20663 ) ) ;
#9798=ORIENTED_EDGE ( 'NONE', *, *, #19239, .F. ) ;
#9837=ADVANCED_FACE ( 'NONE', ( #1501 ), #8936, .T. ) ;
#9912=DIRECTION ( 'NONE',  ( -0.4999999999999916178, 0.000000000000000000, 0.8660254037844433705 ) ) ;
#9921=VECTOR ( 'NONE', #22083, 39.37007874015748854 ) ;
#9959=PLANE ( 'NONE',  #6052 ) ;
#10080=LINE ( 'NONE', #914, #2659 ) ;
#10102=ORIENTED_EDGE ( 'NONE', *, *, #13359, .T. ) ;
#10169=ORIENTED_EDGE ( 'NONE', *, *, #1590, .T. ) ;
#10175=AXIS2_PLACEMENT_3D ( 'NONE', #3392, #1449, #12439 ) ;
#10279=DIRECTION ( 'NONE',  ( -0.8660254037844438146, 0.000000000000000000, -0.4999999999999911737 ) ) ;
#10394=DIRECTION ( 'NONE',  ( 0.8660254037844437036, 0.000000000000000000, 0.4999999999999911737 ) ) ;
#10403=ADVANCED_FACE ( 'NONE', ( #19546 ), #8193, .F. ) ;
#10414=EDGE_CURVE ( 'NONE', #2273, #2833, #23789, .T. ) ;
#10524=ORIENTED_EDGE ( 'NONE', *, *, #6277, .F. ) ;
#10641=VERTEX_POINT ( 'NONE', #5866 ) ;
#10652=FACE_OUTER_BOUND ( 'NONE', #15648, .T. ) ;
#10673=VERTEX_POINT ( 'NONE', #19275 ) ;
#10678=DIRECTION ( 'NONE',  ( 0.8660254037844382635, 0.000000000000000000, 0.5000000000000004441 ) ) ;
#10681=ORIENTED_EDGE ( 'NONE', *, *, #5186, .F. ) ;
#10688=DIRECTION ( 'NONE',  ( 0.000000000000000000, -0.9961946980917454342, -0.08715574274765833240 ) ) ;
#10693=PLANE ( 'NONE',  #17145 ) ;
#10720=PLANE ( 'NONE',  #10175 ) ;
#10733=ADVANCED_FACE ( 'NONE', ( #17690 ), #19516, .T. ) ;
#10762=SHAPE_REPRESENTATION_RELATIONSHIP ( 'NONE' , 'NONE' ,  #11202, #4743 ) ;
#10864=VERTEX_POINT ( 'NONE', #14038 ) ;
#10901=PRODUCT_DEFINITION ( 'UNKNOWN', '', #582, #15817 ) ;
#11010=DIRECTION ( 'NONE',  ( 0.4999999999999916178, 0.000000000000000000, -0.8660254037844433705 ) ) ;
#11031=ORIENTED_EDGE ( 'NONE', *, *, #23749, .T. ) ;
#11108=LINE ( 'NONE', #22074, #23652 ) ;
#11129=CARTESIAN_POINT ( 'NONE',  ( -0.5116234456863466562, 3.856336430858469555, 2.549370209580444691 ) ) ;
#11202=SHAPE_REPRESENTATION ( 'Aloris-BXA-Wedge-R', ( #9127 ), #5239 ) ;
#11207=EDGE_LOOP ( 'NONE', ( #15436, #18393, #6847, #19416 ) ) ;
#11306=FACE_OUTER_BOUND ( 'NONE', #12512, .T. ) ;
#11354=CARTESIAN_POINT ( 'NONE',  ( 0.08808798601665612793, 3.066692553488282957, 3.256612888476066558 ) ) ;
#11396=LINE ( 'NONE', #18828, #15633 ) ;
#11422=MECHANICAL_CONTEXT ( 'NONE', #20566, 'mechanical' ) ;
#11471=LINE ( 'NONE', #7913, #1480 ) ;
#11483=VERTEX_POINT ( 'NONE', #14562 ) ;
#11499=ORIENTED_EDGE ( 'NONE', *, *, #3310, .F. ) ;
#11516=CARTESIAN_POINT ( 'NONE',  ( 0.7108475124358174524, 3.066692553488282957, 2.927961747820534644 ) ) ;
#11554=CARTESIAN_POINT ( 'NONE',  ( -1.133296993574655964, 3.066692553488282957, 2.163426826761001287 ) ) ;
#11556=ORIENTED_EDGE ( 'NONE', *, *, #23749, .F. ) ;
#11580=DIRECTION ( 'NONE',  ( 0.4999999999999941158, 0.000000000000000000, -0.8660254037844420383 ) ) ;
#11581=ORIENTED_EDGE ( 'NONE', *, *, #10414, .T. ) ;
#11653=CARTESIAN_POINT ( 'NONE',  ( -0.5116234456863466562, 3.514980167629567998, 2.949589416182695878 ) ) ;
#11840=ORIENTED_EDGE ( 'NONE', *, *, #18463, .T. ) ;
#11951=DIRECTION ( 'NONE',  ( -0.5000000000000003331, 0.000000000000000000, 0.8660254037844384856 ) ) ;
#12004=ADVANCED_FACE ( 'NONE', ( #21922 ), #10720, .T. ) ;
#12026=EDGE_CURVE ( 'NONE', #13133, #7381, #23859, .T. ) ;
#12050=FACE_OUTER_BOUND ( 'NONE', #6983, .T. ) ;
#12055=CARTESIAN_POINT ( 'NONE',  ( -0.5116234456863466562, 0.9548081934128058723, 2.635972749958888528 ) ) ;
#12061=ORIENTED_EDGE ( 'NONE', *, *, #21901, .T. ) ;
#12087=ORIENTED_EDGE ( 'NONE', *, *, #21353, .F. ) ;
#12264=ORIENTED_EDGE ( 'NONE', *, *, #17219, .F. ) ;
#12267=PRODUCT ( 'Aloris-BXA-Wedge-R', 'Aloris-BXA-Wedge-R', '', ( #11422 ) ) ;
#12289=DIRECTION ( 'NONE',  ( 0.4999999999999901745, 0.000000000000000000, -0.8660254037844443697 ) ) ;
#12307=CARTESIAN_POINT ( 'NONE',  ( 0.08808798601665612793, 0.9548081934128058723, 3.071846948291761414 ) ) ;
#12323=ORIENTED_EDGE ( 'NONE', *, *, #21353, .T. ) ;
#12422=VECTOR ( 'NONE', #18949, 39.37007874015748143 ) ;
#12439=DIRECTION ( 'NONE',  ( 0.4999999999999942268, 0.000000000000000000, -0.8660254037844420383 ) ) ;
#12460=ORIENTED_EDGE ( 'NONE', *, *, #5743, .F. ) ;
#12478=( CONVERSION_BASED_UNIT ( 'INCH', #21729 ) LENGTH_UNIT ( ) NAMED_UNIT ( #15699 ) );
#12490=CARTESIAN_POINT ( 'NONE',  ( -0.5116234456863466562, 3.514980167629567998, 2.549370209580444691 ) ) ;
#12498=VECTOR ( 'NONE', #11010, 39.37007874015748854 ) ;
#12512=EDGE_LOOP ( 'NONE', ( #7747, #17349, #11499, #12061 ) ) ;
#12531=CARTESIAN_POINT ( 'NONE',  ( 0.3860879860166477329, 3.066692553488282957, 2.740461747820544414 ) ) ;
#12611=CARTESIAN_POINT ( 'NONE',  ( -0.5116234456863466562, 0.9548081934128056503, 2.549370209580444691 ) ) ;
#12616=CARTESIAN_POINT ( 'NONE',  ( -0.5116234456863466562, 0.9548081934128058723, 2.635972749958888528 ) ) ;
#12635=CARTESIAN_POINT ( 'NONE',  ( 0.2730879860166530726, 3.066692553488282957, 2.936183489075822717 ) ) ;
#12801=CARTESIAN_POINT ( 'NONE',  ( -0.02441201398334205686, 3.066692553488282957, 3.451468604327566858 ) ) ;
#12855=CARTESIAN_POINT ( 'NONE',  ( -0.5116234456863466562, 2.661589509557314326, 2.549370209580444691 ) ) ;
#12974=CARTESIAN_POINT ( 'NONE',  ( 0.3003475124358241377, 0.9548081934128058723, 3.454202664143258605 ) ) ;
#13005=CARTESIAN_POINT ( 'NONE',  ( 0.08808798601665612793, 3.066692553488282957, 3.256612888476066558 ) ) ;
#13021=DIRECTION ( 'NONE',  ( 0.000000000000000000, -1.000000000000000000, 0.000000000000000000 ) ) ;
#13082=EDGE_CURVE ( 'NONE', #8012, #18459, #17871, .T. ) ;
#13091=DIRECTION ( 'NONE',  ( 0.000000000000000000, 1.000000000000000000, 0.000000000000000000 ) ) ;
#13120=EDGE_CURVE ( 'NONE', #5165, #13148, #9563, .T. ) ;
#13133=VERTEX_POINT ( 'NONE', #1760 ) ;
#13148=VERTEX_POINT ( 'NONE', #9323 ) ;
#13173=ORIENTED_EDGE ( 'NONE', *, *, #124, .T. ) ;
#13198=LINE ( 'NONE', #11354, #22569 ) ;
#13203=CARTESIAN_POINT ( 'NONE',  ( -0.09435543239135868454, -0.003009961218012348859, 2.763260016782451700 ) ) ;
#13207=( BOUNDED_CURVE ( )  B_SPLINE_CURVE ( 2, ( #8658, #21826, #9028 ),
 .UNSPECIFIED., .F., .T. ) 
 B_SPLINE_CURVE_WITH_KNOTS ( ( 3, 3 ),
 ( 0.000000000000000000, 0.005292957132939934278 ),
 .UNSPECIFIED. ) 
 CURVE ( )  GEOMETRIC_REPRESENTATION_ITEM ( )  RATIONAL_B_SPLINE_CURVE ( ( 1.000000000000000000, 0.4999999999999998335, 1.000000000000000000 ) ) 
 REPRESENTATION_ITEM ( '' )  );
#13282=CARTESIAN_POINT ( 'NONE',  ( -0.1060554323913586589, -0.003009961218012348859, 2.783525011231007706 ) ) ;
#13353=ORIENTED_EDGE ( 'NONE', *, *, #24008, .T. ) ;
#13359=EDGE_CURVE ( 'NONE', #8579, #7946, #11396, .T. ) ;
#13378=SHAPE_DEFINITION_REPRESENTATION ( #8550, #11202 ) ;
#13435=VECTOR ( 'NONE', #16957, 39.37007874015748854 ) ;
#13475=LINE ( 'NONE', #2246, #22776 ) ;
#13479=ORIENTED_EDGE ( 'NONE', *, *, #4382, .F. ) ;
#13501=ADVANCED_FACE ( 'NONE', ( #23308 ), #1254, .T. ) ;
#13537=LINE ( 'NONE', #23011, #20831 ) ;
#13546=EDGE_LOOP ( 'NONE', ( #22836, #21063, #16164, #12264, #13173, #16068, #22364, #3414, #17614, #173, #22504 ) ) ;
#13635=ADVANCED_FACE ( 'NONE', ( #23365 ), #23482, .T. ) ;
#13813=ORIENTED_EDGE ( 'NONE', *, *, #22390, .T. ) ;
#13881=VECTOR ( 'NONE', #5857, 39.37007874015748854 ) ;
#13904=ORIENTED_EDGE ( 'NONE', *, *, #19300, .F. ) ;
#13933=DIRECTION ( 'NONE',  ( -0.4985709748471494063, -0.07555085810113112976, 0.8635502596144279952 ) ) ;
#14038=CARTESIAN_POINT ( 'NONE',  ( -0.02441201398334213318, 0.9548081934128058723, 3.266702664143262158 ) ) ;
#14066=DIRECTION ( 'NONE',  ( 0.8651979924482661177, -0.04370253788966846353, 0.4995222938423190540 ) ) ;
#14068=CARTESIAN_POINT ( 'NONE',  ( -0.5116234456863466562, 2.661589509557314326, 2.693707776877850790 ) ) ;
#14119=DIRECTION ( 'NONE',  ( 0.8660254037844384856, 0.000000000000000000, 0.5000000000000003331 ) ) ;
#14254=DIRECTION ( 'NONE',  ( -0.8660254037844434816, 0.000000000000000000, -0.4999999999999913403 ) ) ;
#14293=( LENGTH_UNIT ( ) NAMED_UNIT ( * ) SI_UNIT ( $, .METRE. ) );
#14317=CARTESIAN_POINT ( 'NONE',  ( 0.3860879860166508970, 0.9548081934128058723, 2.555695807636233496 ) ) ;
#14319=CARTESIAN_POINT ( 'NONE',  ( -0.1166234456863465135, 3.066692553488282957, 2.777423565910347225 ) ) ;
#14325=AXIS2_PLACEMENT_3D ( 'NONE', #21722, #13933, #10279 ) ;
#14359=CARTESIAN_POINT ( 'NONE',  ( -0.001863919267180048824, -0.003009961218012348859, 2.816660016782450704 ) ) ;
#14371=DIRECTION ( 'NONE',  ( 0.000000000000000000, -0.9961946980917454342, -0.08715574274765833240 ) ) ;
#14390=LINE ( 'NONE', #8896, #1126 ) ;
#14415=AXIS2_PLACEMENT_3D ( 'NONE', #20027, #14066, #1495 ) ;
#14455=EDGE_CURVE ( 'NONE', #5544, #7946, #9111, .T. ) ;
#14562=CARTESIAN_POINT ( 'NONE',  ( -0.09435543239135868454, 3.514980167629567998, 2.763260016782451700 ) ) ;
#14583=VERTEX_POINT ( 'NONE', #15099 ) ;
#14667=VECTOR ( 'NONE', #4196, 39.37007874015748854 ) ;
#14675=CARTESIAN_POINT ( 'NONE',  ( -0.3566234456863465740, 3.685658299244018998, 2.638859501304836375 ) ) ;
#14744=DIRECTION ( 'NONE',  ( 0.000000000000000000, 0.000000000000000000, 1.000000000000000000 ) ) ;
#14766=CARTESIAN_POINT ( 'NONE',  ( 0.3003475124358241377, 0.9548081934128058723, 3.454202664143258605 ) ) ;
#14780=CARTESIAN_POINT ( 'NONE',  ( -0.1166234456863465552, 3.066692553488282957, 2.711183489075826181 ) ) ;
#14794=ORIENTED_EDGE ( 'NONE', *, *, #3399, .F. ) ;
#14886=DIRECTION ( 'NONE',  ( 0.4999999999999908962, 0.000000000000000000, -0.8660254037844438146 ) ) ;
#14957=DIRECTION ( 'NONE',  ( -0.8660254037844382635, 0.000000000000000000, -0.5000000000000004441 ) ) ;
#15045=CARTESIAN_POINT ( 'NONE',  ( 0.3060819870397865072, 0.9548081934128058723, 2.694270262774470126 ) ) ;
#15099=CARTESIAN_POINT ( 'NONE',  ( -0.5116234456863466562, 3.514980167629567998, 2.722575290337332365 ) ) ;
#15116=LINE ( 'NONE', #21191, #20076 ) ;
#15131=DIRECTION ( 'NONE',  ( -1.000000000000000000, -0.000000000000000000, -0.000000000000000000 ) ) ;
#15182=LINE ( 'NONE', #15423, #16594 ) ;
#15214=VECTOR ( 'NONE', #14744, 39.37007874015748143 ) ;
#15279=LINE ( 'NONE', #15045, #18034 ) ;
#15294=ORIENTED_EDGE ( 'NONE', *, *, #17225, .F. ) ;
#15423=CARTESIAN_POINT ( 'NONE',  ( -0.5116234456863466562, 4.118954363223904735, 3.002430311359389759 ) ) ;
#15436=ORIENTED_EDGE ( 'NONE', *, *, #995, .T. ) ;
#15463=VECTOR ( 'NONE', #18675, 39.37007874015748854 ) ;
#15545=VECTOR ( 'NONE', #14371, 39.37007874015748143 ) ;
#15555=LINE ( 'NONE', #8342, #8888 ) ;
#15633=VECTOR ( 'NONE', #289, 39.37007874015748854 ) ;
#15648=EDGE_LOOP ( 'NONE', ( #16481, #2374, #18339, #8801 ) ) ;
#15699=DIMENSIONAL_EXPONENTS ( 1.000000000000000000, 0.000000000000000000, 0.000000000000000000, 0.000000000000000000, 0.000000000000000000, 0.000000000000000000, 0.000000000000000000 ) ;
#15775=VECTOR ( 'NONE', #21865, 39.37007874015748854 ) ;
#15817=DESIGN_CONTEXT ( 'detailed design', #23355, 'design' ) ;
#15878=CARTESIAN_POINT ( 'NONE',  ( 0.000000000000000000, 0.000000000000000000, 0.000000000000000000 ) ) ;
#15890=CARTESIAN_POINT ( 'NONE',  ( -0.5116234456863466562, 0.6134519301839026495, 2.624425744575095809 ) ) ;
#16013=CARTESIAN_POINT ( 'NONE',  ( -0.5116234456863466562, 3.856336430858469999, 2.734122295721124640 ) ) ;
#16068=ORIENTED_EDGE ( 'NONE', *, *, #10414, .F. ) ;
#16114=PLANE ( 'NONE',  #14325 ) ;
#16120=B_SPLINE_CURVE_WITH_KNOTS ( 'NONE', 3,
 ( #35, #16987, #9311, #5651 ),
 .UNSPECIFIED., .F., .F.,
 ( 4, 4 ),
 ( 0.08935694927272852528, 0.1543853174178342336 ),
 .UNSPECIFIED. ) ;
#16164=ORIENTED_EDGE ( 'NONE', *, *, #12026, .F. ) ;
#16177=EDGE_CURVE ( 'NONE', #3065, #14583, #23590, .T. ) ;
#16210=FACE_OUTER_BOUND ( 'NONE', #9094, .T. ) ;
#16388=CARTESIAN_POINT ( 'NONE',  ( -0.1166234456863465552, 0.9548081934128058723, 2.526417548891521037 ) ) ;
#16443=DIRECTION ( 'NONE',  ( 0.8660254037844434816, 0.000000000000000000, 0.4999999999999915068 ) ) ;
#16481=ORIENTED_EDGE ( 'NONE', *, *, #12026, .T. ) ;
#16493=CARTESIAN_POINT ( 'NONE',  ( -0.001863919267180048824, -0.003009961218012348859, 2.816660016782450704 ) ) ;
#16557=VECTOR ( 'NONE', #2058, 39.37007874015748143 ) ;
#16561=CARTESIAN_POINT ( 'NONE',  ( -0.1166234456863465552, 3.066692553488282957, 2.711183489075826181 ) ) ;
#16584=EDGE_CURVE ( 'NONE', #6836, #17018, #5061, .T. ) ;
#16594=VECTOR ( 'NONE', #3843, 39.37007874015748854 ) ;
#16598=FACE_OUTER_BOUND ( 'NONE', #21155, .T. ) ;
#16611=ADVANCED_FACE ( 'NONE', ( #12050 ), #2873, .T. ) ;
#16649=EDGE_LOOP ( 'NONE', ( #10169, #9427, #23087, #7779 ) ) ;
#16789=EDGE_CURVE ( 'NONE', #18459, #14583, #4201, .T. ) ;
#16810=CARTESIAN_POINT ( 'NONE',  ( -0.1060554323913586589, 3.514980167629567998, 2.783525011231007706 ) ) ;
#16851=CARTESIAN_POINT ( 'NONE',  ( -0.05329418186030111804, -0.01080343630441895492, 2.905739844640345293 ) ) ;
#16874=DIRECTION ( 'NONE',  ( 0.000000000000000000, -0.9961946980917454342, -0.08715574274765833240 ) ) ;
#16957=DIRECTION ( 'NONE',  ( -0.4999999999999916178, 0.000000000000000000, 0.8660254037844433705 ) ) ;
#16987=CARTESIAN_POINT ( 'NONE',  ( -0.3866234456863465452, 2.661589509557314770, 2.621538993229147962 ) ) ;
#17018=VERTEX_POINT ( 'NONE', #14317 ) ;
#17025=DIRECTION ( 'NONE',  ( -0.4985709748471497393, -0.07555085810113111588, 0.8635502596144276621 ) ) ;
#17129=ORIENTED_EDGE ( 'NONE', *, *, #7635, .T. ) ;
#17145=AXIS2_PLACEMENT_3D ( 'NONE', #22500, #13021, #18608 ) ;
#17198=ORIENTED_EDGE ( 'NONE', *, *, #13082, .T. ) ;
#17219=EDGE_CURVE ( 'NONE', #17018, #13133, #15279, .T. ) ;
#17225=EDGE_CURVE ( 'NONE', #21966, #8012, #22467, .T. ) ;
#17259=VECTOR ( 'NONE', #20638, 39.37007874015748854 ) ;
#17261=ORIENTED_EDGE ( 'NONE', *, *, #18463, .F. ) ;
#17321=CARTESIAN_POINT ( 'NONE',  ( -0.3066867353193435397, 0.9548081934128058723, 2.155722135785137716 ) ) ;
#17349=ORIENTED_EDGE ( 'NONE', *, *, #5269, .F. ) ;
#17368=CARTESIAN_POINT ( 'NONE',  ( 0.7108475124358174524, 0.9548081934128058723, 2.743195807636230388 ) ) ;
#17385=CARTESIAN_POINT ( 'NONE',  ( 0.08808798601665612793, 3.066692553488282957, 3.256612888476066558 ) ) ;
#17596=ADVANCED_FACE ( 'NONE', ( #16598 ), #24018, .T. ) ;
#17614=ORIENTED_EDGE ( 'NONE', *, *, #18374, .F. ) ;
#17623=PLANE ( 'NONE',  #7720 ) ;
#17634=EDGE_CURVE ( 'NONE', #18353, #8579, #2074, .T. ) ;
#17647=VECTOR ( 'NONE', #321, 39.37007874015747433 ) ;
#17690=FACE_OUTER_BOUND ( 'NONE', #6869, .T. ) ;
#17846=CARTESIAN_POINT ( 'NONE',  ( -0.5116234456863466562, 0.7841300617983542054, 2.630199247266991947 ) ) ;
#17871=LINE ( 'NONE', #21518, #7788 ) ;
#17996=ORIENTED_EDGE ( 'NONE', *, *, #17634, .T. ) ;
#18032=CARTESIAN_POINT ( 'NONE',  ( 0.000000000000000000, 3.514980167629567998, 0.000000000000000000 ) ) ;
#18034=VECTOR ( 'NONE', #9912, 39.37007874015748854 ) ;
#18062=DIRECTION ( 'NONE',  ( 0.8660254037844382635, 0.000000000000000000, 0.5000000000000004441 ) ) ;
#18078=CARTESIAN_POINT ( 'NONE',  ( -0.4416234456863467051, 0.7841300617983542054, 2.589784728423718096 ) ) ;
#18153=CARTESIAN_POINT ( 'NONE',  ( 0.3530939849935142982, 0.9548081934128058723, 2.797609033937592304 ) ) ;
#18201=CARTESIAN_POINT ( 'NONE',  ( -0.3616234456863465785, 3.514980167629567998, 2.635972749958888528 ) ) ;
#18286=AXIS2_PLACEMENT_3D ( 'NONE', #18032, #1687, #9122 ) ;
#18309=AXIS2_PLACEMENT_3D ( 'NONE', #5394, #23793, #7115 ) ;
#18310=( NAMED_UNIT ( * ) PLANE_ANGLE_UNIT ( ) SI_UNIT ( $, .RADIAN. ) );
#18339=ORIENTED_EDGE ( 'NONE', *, *, #4227, .F. ) ;
#18353=VERTEX_POINT ( 'NONE', #20568 ) ;
#18374=EDGE_CURVE ( 'NONE', #10673, #2652, #1552, .T. ) ;
#18393=ORIENTED_EDGE ( 'NONE', *, *, #16177, .T. ) ;
#18459=VERTEX_POINT ( 'NONE', #6288 ) ;
#18463=EDGE_CURVE ( 'NONE', #9585, #18353, #443, .T. ) ;
#18531=ORIENTED_EDGE ( 'NONE', *, *, #5743, .T. ) ;
#18542=LINE ( 'NONE', #1832, #2713 ) ;
#18548=LINE ( 'NONE', #13203, #23904 ) ;
#18608=DIRECTION ( 'NONE',  ( 0.000000000000000000, 0.000000000000000000, 1.000000000000000000 ) ) ;
#18675=DIRECTION ( 'NONE',  ( 0.03777542905056541916, -0.9971419496943164651, -0.06542896239329260011 ) ) ;
#18828=CARTESIAN_POINT ( 'NONE',  ( -1.144996993574672217, 3.066692553488282957, 2.183691821209530648 ) ) ;
#18835=ORIENTED_EDGE ( 'NONE', *, *, #21901, .F. ) ;
#18848=LINE ( 'NONE', #7511, #22201 ) ;
#18949=DIRECTION ( 'NONE',  ( -0.8660254037844526964, 0.000000000000000000, -0.4999999999999756306 ) ) ;
#19138=ORIENTED_EDGE ( 'NONE', *, *, #3399, .T. ) ;
#19195=VECTOR ( 'NONE', #423, 39.37007874015748143 ) ;
#19199=ORIENTED_EDGE ( 'NONE', *, *, #24008, .F. ) ;
#19209=VECTOR ( 'NONE', #5966, 39.37007874015747433 ) ;
#19239=EDGE_CURVE ( 'NONE', #14583, #20092, #13207, .T. ) ;
#19275=CARTESIAN_POINT ( 'NONE',  ( -0.5116234456863466562, 0.9548081934128057613, 2.725603391761944660 ) ) ;
#19300=EDGE_CURVE ( 'NONE', #7081, #5165, #2936, .T. ) ;
#19416=ORIENTED_EDGE ( 'NONE', *, *, #24068, .T. ) ;
#19441=ADVANCED_FACE ( 'NONE', ( #3535 ), #9631, .T. ) ;
#19463=DIRECTION ( 'NONE',  ( 0.8660254037844443697, 0.000000000000000000, 0.4999999999999901745 ) ) ;
#19473=UNCERTAINTY_MEASURE_WITH_UNIT (LENGTH_MEASURE( 1.000000000000000082E-05 ), #12478, 'distance_accuracy_value', 'NONE');
#19516=PLANE ( 'NONE',  #23364 ) ;
#19546=FACE_OUTER_BOUND ( 'NONE', #11207, .T. ) ;
#19588=ORIENTED_EDGE ( 'NONE', *, *, #4227, .T. ) ;
#19616=EDGE_LOOP ( 'NONE', ( #22729, #11556, #24019, #5863 ) ) ;
#19738=ORIENTED_EDGE ( 'NONE', *, *, #17634, .F. ) ;
#19851=ADVANCED_FACE ( 'NONE', ( #7293 ), #3623, .T. ) ;
#19911=CARTESIAN_POINT ( 'NONE',  ( -0.5116234456863466562, 0.7841300617983539833, 2.549370209580444691 ) ) ;
#20027=CARTESIAN_POINT ( 'NONE',  ( 0.3003475124358242487, 3.066692553488282957, 3.638968604327563749 ) ) ;
#20029=CARTESIAN_POINT ( 'NONE',  ( -0.4516234456863466584, 0.4427737985694512046, 2.584011225731822403 ) ) ;
#20076=VECTOR ( 'NONE', #5950, 39.37007874015748143 ) ;
#20092=VERTEX_POINT ( 'NONE', #4469 ) ;
#20158=VECTOR ( 'NONE', #4232, 39.37007874015748143 ) ;
#20228=PLANE ( 'NONE',  #18286 ) ;
#20252=ORIENTED_EDGE ( 'NONE', *, *, #6277, .T. ) ;
#20272=CARTESIAN_POINT ( 'NONE',  ( -0.3516234456863465696, 3.856336430858469999, 2.641746252650784665 ) ) ;
#20294=ORIENTED_EDGE ( 'NONE', *, *, #13082, .F. ) ;
#20303=FACE_OUTER_BOUND ( 'NONE', #4302, .T. ) ;
#20420=VECTOR ( 'NONE', #20497, 39.37007874015748143 ) ;
#20497=DIRECTION ( 'NONE',  ( 0.000000000000000000, -0.9961946980917454342, -0.08715574274765833240 ) ) ;
#20540=AXIS2_PLACEMENT_3D ( 'NONE', #21621, #21745, #3093 ) ;
#20566=APPLICATION_CONTEXT ( 'configuration controlled 3d designs of mechanical parts and assemblies' ) ;
#20568=CARTESIAN_POINT ( 'NONE',  ( -0.09435543239135868454, 3.066692553488282957, 2.763260016782451700 ) ) ;
#20625=EDGE_CURVE ( 'NONE', #20092, #7867, #1484, .T. ) ;
#20638=DIRECTION ( 'NONE',  ( -0.5000000000000003331, 0.000000000000000000, 0.8660254037844384856 ) ) ;
#20650=EDGE_CURVE ( 'NONE', #10641, #2833, #20855, .T. ) ;
#20663=ORIENTED_EDGE ( 'NONE', *, *, #8582, .T. ) ;
#20688=VECTOR ( 'NONE', #22611, 39.37007874015748143 ) ;
#20767=ORIENTED_EDGE ( 'NONE', *, *, #19300, .T. ) ;
#20784=AXIS2_PLACEMENT_3D ( 'NONE', #22305, #9267, #14886 ) ;
#20803=DIRECTION ( 'NONE',  ( 0.000000000000000000, 1.000000000000000000, 0.000000000000000000 ) ) ;
#20831=VECTOR ( 'NONE', #11580, 39.37007874015748143 ) ;
#20855=LINE ( 'NONE', #2330, #20420 ) ;
#20899=CARTESIAN_POINT ( 'NONE',  ( 0.3860879860166477329, 3.066692553488282957, 2.740461747820544414 ) ) ;
#20903=LINE ( 'NONE', #3960, #14667 ) ;
#21063=ORIENTED_EDGE ( 'NONE', *, *, #22252, .F. ) ;
#21127=EDGE_CURVE ( 'NONE', #10864, #2273, #23799, .T. ) ;
#21155=EDGE_LOOP ( 'NONE', ( #6679, #1494, #8275, #17129 ) ) ;
#21163=AXIS2_PLACEMENT_3D ( 'NONE', #14780, #15131, #4140 ) ;
#21184=VERTEX_POINT ( 'NONE', #4791 ) ;
#21191=CARTESIAN_POINT ( 'NONE',  ( -0.5116234456863466562, 0.9548081934128058723, 2.754369331946250110 ) ) ;
#21304=CARTESIAN_POINT ( 'NONE',  ( -0.4366234456863467006, 0.9548081934128058723, 2.592671479769666387 ) ) ;
#21353=EDGE_CURVE ( 'NONE', #6836, #21772, #4390, .T. ) ;
#21518=CARTESIAN_POINT ( 'NONE',  ( -0.1868639192671823768, 3.514980167629567998, 3.137089416182696766 ) ) ;
#21573=VECTOR ( 'NONE', #18062, 39.37007874015748854 ) ;
#21593=ORIENTED_EDGE ( 'NONE', *, *, #8468, .F. ) ;
#21616=CARTESIAN_POINT ( 'NONE',  ( -0.5116234456863466562, 0.4427737985694510381, 2.549370209580444691 ) ) ;
#21621=CARTESIAN_POINT ( 'NONE',  ( 0.2730879860166530726, 3.066692553488282957, 2.936183489075822717 ) ) ;
#21722=CARTESIAN_POINT ( 'NONE',  ( -0.5116234456863466562, 3.066692553488282957, 2.910369331946250249 ) ) ;
#21729=LENGTH_MEASURE_WITH_UNIT ( LENGTH_MEASURE( 0.02539999999999999897 ), #14293 );
#21745=DIRECTION ( 'NONE',  ( 0.4985709748471496838, 0.07555085810113111588, -0.8635502596144277732 ) ) ;
#21756=VECTOR ( 'NONE', #13091, 39.37007874015748143 ) ;
#21772=VERTEX_POINT ( 'NONE', #12635 ) ;
#21804=LINE ( 'NONE', #8750, #15545 ) ;
#21826=CARTESIAN_POINT ( 'NONE',  ( -0.5116234456863468782, 3.514980167629567998, 2.549370209580444246 ) ) ;
#21865=DIRECTION ( 'NONE',  ( 0.8660254037844434816, 0.000000000000000000, 0.4999999999999916178 ) ) ;
#21887=VERTEX_POINT ( 'NONE', #283 ) ;
#21901=EDGE_CURVE ( 'NONE', #13148, #10864, #13475, .T. ) ;
#21922=FACE_OUTER_BOUND ( 'NONE', #2523, .T. ) ;
#21966=VERTEX_POINT ( 'NONE', #22605 ) ;
#22003=DIRECTION ( 'NONE',  ( 0.5000000000000005551, 0.000000000000000000, -0.8660254037844383745 ) ) ;
#22008=ORIENTED_EDGE ( 'NONE', *, *, #18374, .T. ) ;
#22074=CARTESIAN_POINT ( 'NONE',  ( 0.2730879860166530726, 3.066692553488282957, 2.936183489075822717 ) ) ;
#22083=DIRECTION ( 'NONE',  ( 0.8660254037844443697, 0.000000000000000000, 0.4999999999999901745 ) ) ;
#22201=VECTOR ( 'NONE', #14957, 39.37007874015748854 ) ;
#22252=EDGE_CURVE ( 'NONE', #7381, #5448, #22295, .T. ) ;
#22281=CARTESIAN_POINT ( 'NONE',  ( -0.5116234456863466562, 2.661589509557312994, 2.693707776877850790 ) ) ;
#22295=LINE ( 'NONE', #1695, #16557 ) ;
#22305=CARTESIAN_POINT ( 'NONE',  ( 0.08808798601665612793, 3.066692553488282957, 3.256612888476066558 ) ) ;
#22346=VECTOR ( 'NONE', #10394, 39.37007874015748854 ) ;
#22364=ORIENTED_EDGE ( 'NONE', *, *, #21127, .F. ) ;
#22390=EDGE_CURVE ( 'NONE', #7867, #11483, #13537, .T. ) ;
#22442=EDGE_CURVE ( 'NONE', #3065, #10673, #15116, .T. ) ;
#22467=LINE ( 'NONE', #5767, #17259 ) ;
#22500=CARTESIAN_POINT ( 'NONE',  ( 0.000000000000000000, 3.066692553488282957, 0.2004988538245859597 ) ) ;
#22504=ORIENTED_EDGE ( 'NONE', *, *, #995, .F. ) ;
#22569=VECTOR ( 'NONE', #6090, 39.37007874015748143 ) ;
#22602=ORIENTED_EDGE ( 'NONE', *, *, #20625, .T. ) ;
#22604=AXIS2_PLACEMENT_3D ( 'NONE', #14359, #14119, #11951 ) ;
#22605=CARTESIAN_POINT ( 'NONE',  ( -0.001863919267180048824, 3.514980167629567998, 2.816660016782450704 ) ) ;
#22611=DIRECTION ( 'NONE',  ( -0.4999999999999909517, 0.000000000000000000, 0.8660254037844438146 ) ) ;
#22638=DIRECTION ( 'NONE',  ( -0.8660254037844434816, 0.000000000000000000, -0.4999999999999915068 ) ) ;
#22681=( BOUNDED_CURVE ( )  B_SPLINE_CURVE ( 2, ( #21304, #4597, #12055 ),
 .UNSPECIFIED., .F., .F. ) 
 B_SPLINE_CURVE_WITH_KNOTS ( ( 3, 3 ),
 ( 1.734723475976807094E-18, 0.002646478566469958466 ),
 .UNSPECIFIED. ) 
 CURVE ( )  GEOMETRIC_REPRESENTATION_ITEM ( )  RATIONAL_B_SPLINE_CURVE ( ( 1.000000000000000000, 0.4999999999999997780, 1.000000000000000000 ) ) 
 REPRESENTATION_ITEM ( '' )  );
#22727=ADVANCED_FACE ( 'NONE', ( #11306 ), #9959, .T. ) ;
#22729=ORIENTED_EDGE ( 'NONE', *, *, #22442, .T. ) ;
#22776=VECTOR ( 'NONE', #16874, 39.37007874015748143 ) ;
#22779=ORIENTED_EDGE ( 'NONE', *, *, #17219, .T. ) ;
#22797=CARTESIAN_POINT ( 'NONE',  ( -0.1060554323913586589, 3.066692553488282957, 2.783525011231007706 ) ) ;
#22836=ORIENTED_EDGE ( 'NONE', *, *, #9659, .F. ) ;
#22904=ORIENTED_EDGE ( 'NONE', *, *, #1590, .F. ) ;
#23011=CARTESIAN_POINT ( 'NONE',  ( -0.1060554323913586589, 3.514980167629567998, 2.783525011231007706 ) ) ;
#23069=EDGE_LOOP ( 'NONE', ( #19738, #17261, #21593, #20767, #8340, #23761, #20252, #18531, #12323, #19588, #2984, #7168 ) ) ;
#23087=ORIENTED_EDGE ( 'NONE', *, *, #6038, .T. ) ;
#23093=FACE_OUTER_BOUND ( 'NONE', #13546, .T. ) ;
#23112=ADVANCED_FACE ( 'NONE', ( #20303 ), #8836, .T. ) ;
#23181=DIRECTION ( 'NONE',  ( 0.000000000000000000, 0.000000000000000000, 1.000000000000000000 ) ) ;
#23294=DIRECTION ( 'NONE',  ( 1.000000000000000000, 0.000000000000000000, 0.000000000000000000 ) ) ;
#23308=FACE_OUTER_BOUND ( 'NONE', #4907, .T. ) ;
#23310=CARTESIAN_POINT ( 'NONE',  ( -0.5116234456863466562, 1.808198851485059988, 2.664840263418369659 ) ) ;
#23355=APPLICATION_CONTEXT ( 'configuration controlled 3d designs of mechanical parts and assemblies' ) ;
#23364=AXIS2_PLACEMENT_3D ( 'NONE', #8412, #8537, #23400 ) ;
#23365=FACE_OUTER_BOUND ( 'NONE', #16649, .T. ) ;
#23400=DIRECTION ( 'NONE',  ( 0.8660254037844526964, 0.000000000000000000, 0.4999999999999757416 ) ) ;
#23431=CARTESIAN_POINT ( 'NONE',  ( -0.5116234456863466562, 4.027014562472920112, 2.739895798413020778 ) ) ;
#23482=PLANE ( 'NONE',  #22604 ) ;
#23525=ORIENTED_EDGE ( 'NONE', *, *, #16789, .F. ) ;
#23590=B_SPLINE_CURVE_WITH_KNOTS ( 'NONE', 3,
 ( #7414, #1679, #22281, #9112 ),
 .UNSPECIFIED., .F., .F.,
 ( 4, 4 ),
 ( 0.02432858112762273373, 0.08935694927272852528 ),
 .UNSPECIFIED. ) ;
#23652=VECTOR ( 'NONE', #1713, 39.37007874015748854 ) ;
#23680=CARTESIAN_POINT ( 'NONE',  ( -0.1868639192671821270, 3.514980167629567998, 3.137089416182696322 ) ) ;
#23741=EDGE_CURVE ( 'NONE', #2652, #10864, #20903, .T. ) ;
#23749=EDGE_CURVE ( 'NONE', #18459, #10673, #15182, .T. ) ;
#23761=ORIENTED_EDGE ( 'NONE', *, *, #3310, .T. ) ;
#23789=LINE ( 'NONE', #12974, #12498 ) ;
#23793=DIRECTION ( 'NONE',  ( -1.000000000000000000, -0.000000000000000000, -0.000000000000000000 ) ) ;
#23799=LINE ( 'NONE', #7120, #15775 ) ;
#23859=LINE ( 'NONE', #18153, #3543 ) ;
#23898=DIRECTION ( 'NONE',  ( 0.000000000000000000, 1.000000000000000000, 0.000000000000000000 ) ) ;
#23904=VECTOR ( 'NONE', #23898, 39.37007874015748143 ) ;
#23927=EDGE_CURVE ( 'NONE', #11483, #21966, #24025, .T. ) ;
#24008=EDGE_CURVE ( 'NONE', #18353, #11483, #18548, .T. ) ;
#24010=ORIENTED_EDGE ( 'NONE', *, *, #23741, .T. ) ;
#24018=PLANE ( 'NONE',  #21163 ) ;
#24019=ORIENTED_EDGE ( 'NONE', *, *, #16789, .T. ) ;
#24025=LINE ( 'NONE', #5745, #9921 ) ;
#24034=LINE ( 'NONE', #16851, #15463 ) ;
#24068=EDGE_CURVE ( 'NONE', #20092, #21184, #16120, .T. ) ;
#24100=CARTESIAN_POINT ( 'NONE',  ( -0.1698811246235177597, 3.066692553488282957, 3.107674353005361212 ) ) ;
#24138=COLOUR_RGB('Deep Blue', 0.66274510, 0.83137255, 0.94901961);
#24139=FILL_AREA_STYLE_COLOUR('',#24138);
#24140=FILL_AREA_STYLE('',(#24139));
#24141=SURFACE_STYLE_FILL_AREA(#24140);
#24142=SURFACE_SIDE_STYLE('',(#24141));
#24143=SURFACE_STYLE_USAGE(.BOTH.,#24142);
#24144=PRESENTATION_STYLE_ASSIGNMENT((#24143));
#24180=STYLED_ITEM('',(#24144),#1044);
#24181=MECHANICAL_DESIGN_GEOMETRIC_PRESENTATION_REPRESENTATION('',(#24180),#5239);
ENDSEC;
END-ISO-10303-21;
